ISO-10303-21;
HEADER;
/* Generated by software containing ST-Developer
 * from STEP Tools, Inc. (www.steptools.com) 
 */

FILE_DESCRIPTION(
/* description */ ('Door-style hinge test fixture with detent'),
/* implementation_level */ '2;1');

FILE_NAME(
/* name */ 'Bearing retaining cap (1).step',
/* time_stamp */ '2026-10-28T03:24:57-07:00',
/* author */ (''),
/* organization */ (''),
/* preprocessor_version */ 'ST-DEVELOPER v20.2',
/* originating_system */ 'Autodesk Translation Framework v15.17.0.0',
/* authorisation */ '');

FILE_SCHEMA (('AUTOMOTIVE_DESIGN { 1 0 10303 214 3 1 1 }'));
ENDSEC;

DATA;
#10=MECHANICAL_DESIGN_GEOMETRIC_PRESENTATION_REPRESENTATION('',(#331),#9813);
#268=SHAPE_REPRESENTATION_RELATIONSHIP('SRR','None',#9945,#299);
#299=ADVANCED_BREP_SHAPE_REPRESENTATION('',(#371),#9788);
#331=STYLED_ITEM('',(#10183),#371);
#371=MANIFOLD_SOLID_BREP('Body1',#4762);
#449=FACE_BOUND('',#1085,.T.);
#450=FACE_BOUND('',#1088,.T.);
#451=FACE_BOUND('',#1091,.T.);
#452=FACE_BOUND('',#1093,.T.);
#453=FACE_BOUND('',#1100,.T.);
#454=FACE_BOUND('',#1101,.T.);
#455=FACE_BOUND('',#1102,.T.);
#456=FACE_BOUND('',#1103,.T.);
#553=PLANE('',#5307);
#554=PLANE('',#5313);
#555=PLANE('',#5319);
#556=PLANE('',#5322);
#557=PLANE('',#5338);
#748=FACE_OUTER_BOUND('',#1083,.T.);
#749=FACE_OUTER_BOUND('',#1084,.T.);
#750=FACE_OUTER_BOUND('',#1086,.T.);
#751=FACE_OUTER_BOUND('',#1087,.T.);
#752=FACE_OUTER_BOUND('',#1089,.T.);
#753=FACE_OUTER_BOUND('',#1090,.T.);
#754=FACE_OUTER_BOUND('',#1092,.T.);
#755=FACE_OUTER_BOUND('',#1094,.T.);
#756=FACE_OUTER_BOUND('',#1095,.T.);
#757=FACE_OUTER_BOUND('',#1096,.T.);
#758=FACE_OUTER_BOUND('',#1097,.T.);
#759=FACE_OUTER_BOUND('',#1098,.T.);
#760=FACE_OUTER_BOUND('',#1099,.T.);
#1083=EDGE_LOOP('',(#3597,#3598,#3599,#3600));
#1084=EDGE_LOOP('',(#3601,#3602));
#1085=EDGE_LOOP('',(#3603));
#1086=EDGE_LOOP('',(#3604,#3605,#3606,#3607));
#1087=EDGE_LOOP('',(#3608,#3609));
#1088=EDGE_LOOP('',(#3610));
#1089=EDGE_LOOP('',(#3611,#3612,#3613,#3614));
#1090=EDGE_LOOP('',(#3615,#3616));
#1091=EDGE_LOOP('',(#3617));
#1092=EDGE_LOOP('',(#3618,#3619,#3620,#3621,#3622,#3623,#3624));
#1093=EDGE_LOOP('',(#3625));
#1094=EDGE_LOOP('',(#3626,#3627,#3628,#3629));
#1095=EDGE_LOOP('',(#3630,#3631,#3632,#3633));
#1096=EDGE_LOOP('',(#3634,#3635,#3636,#3637));
#1097=EDGE_LOOP('',(#3638,#3639,#3640,#3641));
#1098=EDGE_LOOP('',(#3642,#3643,#3644,#3645,#3646,#3647,#3648,#3649,#3650,
#3651,#3652,#3653,#3654,#3655,#3656,#3657));
#1099=EDGE_LOOP('',(#3658));
#1100=EDGE_LOOP('',(#3659));
#1101=EDGE_LOOP('',(#3660));
#1102=EDGE_LOOP('',(#3661));
#1103=EDGE_LOOP('',(#3662));
#1459=LINE('',#7721,#1779);
#1460=LINE('',#7725,#1780);
#1461=LINE('',#7734,#1781);
#1462=LINE('',#7738,#1782);
#1463=LINE('',#7747,#1783);
#1464=LINE('',#7751,#1784);
#1465=LINE('',#7767,#1785);
#1466=LINE('',#7771,#1786);
#1467=LINE('',#7775,#1787);
#1468=LINE('',#7780,#1788);
#1469=LINE('',#7784,#1789);
#1779=VECTOR('',#6210,1.);
#1780=VECTOR('',#6213,1.);
#1781=VECTOR('',#6224,1.);
#1782=VECTOR('',#6227,1.);
#1783=VECTOR('',#6238,1.);
#1784=VECTOR('',#6241,1.);
#1785=VECTOR('',#6264,0.225);
#1786=VECTOR('',#6269,0.225);
#1787=VECTOR('',#6274,0.225);
#1788=VECTOR('',#6281,1.02);
#1789=VECTOR('',#6286,2.1);
#2044=CIRCLE('',#5305,0.375);
#2045=CIRCLE('',#5306,0.375);
#2046=CIRCLE('',#5308,2.1);
#2047=CIRCLE('',#5309,0.225);
#2048=CIRCLE('',#5311,0.375);
#2049=CIRCLE('',#5312,0.375);
#2050=CIRCLE('',#5314,2.1);
#2051=CIRCLE('',#5315,0.225);
#2052=CIRCLE('',#5317,0.375);
#2053=CIRCLE('',#5318,0.375);
#2054=CIRCLE('',#5320,2.1);
#2055=CIRCLE('',#5321,0.225);
#2056=CIRCLE('',#5323,2.1);
#2057=CIRCLE('',#5324,2.1);
#2058=CIRCLE('',#5325,2.1);
#2059=CIRCLE('',#5326,2.1);
#2060=CIRCLE('',#5327,1.02);
#2061=CIRCLE('',#5329,0.225);
#2062=CIRCLE('',#5331,0.225);
#2063=CIRCLE('',#5333,0.225);
#2064=CIRCLE('',#5335,1.02);
#2065=CIRCLE('',#5337,2.1);
#2351=VERTEX_POINT('',#7719);
#2352=VERTEX_POINT('',#7720);
#2353=VERTEX_POINT('',#7722);
#2354=VERTEX_POINT('',#7724);
#2355=VERTEX_POINT('',#7729);
#2356=VERTEX_POINT('',#7732);
#2357=VERTEX_POINT('',#7733);
#2358=VERTEX_POINT('',#7735);
#2359=VERTEX_POINT('',#7737);
#2360=VERTEX_POINT('',#7742);
#2361=VERTEX_POINT('',#7745);
#2362=VERTEX_POINT('',#7746);
#2363=VERTEX_POINT('',#7748);
#2364=VERTEX_POINT('',#7750);
#2365=VERTEX_POINT('',#7755);
#2366=VERTEX_POINT('',#7759);
#2367=VERTEX_POINT('',#7763);
#2368=VERTEX_POINT('',#7766);
#2369=VERTEX_POINT('',#7770);
#2370=VERTEX_POINT('',#7774);
#2371=VERTEX_POINT('',#7778);
#2372=VERTEX_POINT('',#7782);
#2815=EDGE_CURVE('',#2351,#2352,#1459,.T.);
#2816=EDGE_CURVE('',#2351,#2353,#2044,.T.);
#2817=EDGE_CURVE('',#2354,#2353,#1460,.T.);
#2818=EDGE_CURVE('',#2352,#2354,#2045,.T.);
#2819=EDGE_CURVE('',#2353,#2351,#2046,.T.);
#2820=EDGE_CURVE('',#2355,#2355,#2047,.T.);
#2821=EDGE_CURVE('',#2356,#2357,#1461,.T.);
#2822=EDGE_CURVE('',#2356,#2358,#2048,.T.);
#2823=EDGE_CURVE('',#2359,#2358,#1462,.T.);
#2824=EDGE_CURVE('',#2357,#2359,#2049,.T.);
#2825=EDGE_CURVE('',#2358,#2356,#2050,.T.);
#2826=EDGE_CURVE('',#2360,#2360,#2051,.T.);
#2827=EDGE_CURVE('',#2361,#2362,#1463,.T.);
#2828=EDGE_CURVE('',#2361,#2363,#2052,.T.);
#2829=EDGE_CURVE('',#2364,#2363,#1464,.T.);
#2830=EDGE_CURVE('',#2362,#2364,#2053,.T.);
#2831=EDGE_CURVE('',#2363,#2361,#2054,.T.);
#2832=EDGE_CURVE('',#2365,#2365,#2055,.T.);
#2833=EDGE_CURVE('',#2362,#2354,#2056,.T.);
#2834=EDGE_CURVE('',#2366,#2364,#2057,.T.);
#2835=EDGE_CURVE('',#2357,#2366,#2058,.T.);
#2836=EDGE_CURVE('',#2352,#2359,#2059,.T.);
#2837=EDGE_CURVE('',#2367,#2367,#2060,.T.);
#2838=EDGE_CURVE('',#2355,#2368,#1465,.T.);
#2839=EDGE_CURVE('',#2368,#2368,#2061,.T.);
#2840=EDGE_CURVE('',#2360,#2369,#1466,.T.);
#2841=EDGE_CURVE('',#2369,#2369,#2062,.T.);
#2842=EDGE_CURVE('',#2365,#2370,#1467,.T.);
#2843=EDGE_CURVE('',#2370,#2370,#2063,.T.);
#2844=EDGE_CURVE('',#2371,#2371,#2064,.T.);
#2845=EDGE_CURVE('',#2371,#2367,#1468,.T.);
#2846=EDGE_CURVE('',#2372,#2372,#2065,.T.);
#2847=EDGE_CURVE('',#2372,#2366,#1469,.T.);
#3597=ORIENTED_EDGE('',*,*,#2815,.F.);
#3598=ORIENTED_EDGE('',*,*,#2816,.T.);
#3599=ORIENTED_EDGE('',*,*,#2817,.F.);
#3600=ORIENTED_EDGE('',*,*,#2818,.F.);
#3601=ORIENTED_EDGE('',*,*,#2819,.F.);
#3602=ORIENTED_EDGE('',*,*,#2816,.F.);
#3603=ORIENTED_EDGE('',*,*,#2820,.F.);
#3604=ORIENTED_EDGE('',*,*,#2821,.F.);
#3605=ORIENTED_EDGE('',*,*,#2822,.T.);
#3606=ORIENTED_EDGE('',*,*,#2823,.F.);
#3607=ORIENTED_EDGE('',*,*,#2824,.F.);
#3608=ORIENTED_EDGE('',*,*,#2825,.F.);
#3609=ORIENTED_EDGE('',*,*,#2822,.F.);
#3610=ORIENTED_EDGE('',*,*,#2826,.F.);
#3611=ORIENTED_EDGE('',*,*,#2827,.F.);
#3612=ORIENTED_EDGE('',*,*,#2828,.T.);
#3613=ORIENTED_EDGE('',*,*,#2829,.F.);
#3614=ORIENTED_EDGE('',*,*,#2830,.F.);
#3615=ORIENTED_EDGE('',*,*,#2831,.F.);
#3616=ORIENTED_EDGE('',*,*,#2828,.F.);
#3617=ORIENTED_EDGE('',*,*,#2832,.F.);
#3618=ORIENTED_EDGE('',*,*,#2818,.T.);
#3619=ORIENTED_EDGE('',*,*,#2833,.F.);
#3620=ORIENTED_EDGE('',*,*,#2830,.T.);
#3621=ORIENTED_EDGE('',*,*,#2834,.F.);
#3622=ORIENTED_EDGE('',*,*,#2835,.F.);
#3623=ORIENTED_EDGE('',*,*,#2824,.T.);
#3624=ORIENTED_EDGE('',*,*,#2836,.F.);
#3625=ORIENTED_EDGE('',*,*,#2837,.F.);
#3626=ORIENTED_EDGE('',*,*,#2820,.T.);
#3627=ORIENTED_EDGE('',*,*,#2838,.T.);
#3628=ORIENTED_EDGE('',*,*,#2839,.F.);
#3629=ORIENTED_EDGE('',*,*,#2838,.F.);
#3630=ORIENTED_EDGE('',*,*,#2826,.T.);
#3631=ORIENTED_EDGE('',*,*,#2840,.T.);
#3632=ORIENTED_EDGE('',*,*,#2841,.F.);
#3633=ORIENTED_EDGE('',*,*,#2840,.F.);
#3634=ORIENTED_EDGE('',*,*,#2832,.T.);
#3635=ORIENTED_EDGE('',*,*,#2842,.T.);
#3636=ORIENTED_EDGE('',*,*,#2843,.F.);
#3637=ORIENTED_EDGE('',*,*,#2842,.F.);
#3638=ORIENTED_EDGE('',*,*,#2844,.F.);
#3639=ORIENTED_EDGE('',*,*,#2845,.T.);
#3640=ORIENTED_EDGE('',*,*,#2837,.T.);
#3641=ORIENTED_EDGE('',*,*,#2845,.F.);
#3642=ORIENTED_EDGE('',*,*,#2846,.F.);
#3643=ORIENTED_EDGE('',*,*,#2847,.T.);
#3644=ORIENTED_EDGE('',*,*,#2834,.T.);
#3645=ORIENTED_EDGE('',*,*,#2829,.T.);
#3646=ORIENTED_EDGE('',*,*,#2831,.T.);
#3647=ORIENTED_EDGE('',*,*,#2827,.T.);
#3648=ORIENTED_EDGE('',*,*,#2833,.T.);
#3649=ORIENTED_EDGE('',*,*,#2817,.T.);
#3650=ORIENTED_EDGE('',*,*,#2819,.T.);
#3651=ORIENTED_EDGE('',*,*,#2815,.T.);
#3652=ORIENTED_EDGE('',*,*,#2836,.T.);
#3653=ORIENTED_EDGE('',*,*,#2823,.T.);
#3654=ORIENTED_EDGE('',*,*,#2825,.T.);
#3655=ORIENTED_EDGE('',*,*,#2821,.T.);
#3656=ORIENTED_EDGE('',*,*,#2835,.T.);
#3657=ORIENTED_EDGE('',*,*,#2847,.F.);
#3658=ORIENTED_EDGE('',*,*,#2846,.T.);
#3659=ORIENTED_EDGE('',*,*,#2839,.T.);
#3660=ORIENTED_EDGE('',*,*,#2841,.T.);
#3661=ORIENTED_EDGE('',*,*,#2843,.T.);
#3662=ORIENTED_EDGE('',*,*,#2844,.T.);
#4413=CYLINDRICAL_SURFACE('',#5304,0.375);
#4414=CYLINDRICAL_SURFACE('',#5310,0.375);
#4415=CYLINDRICAL_SURFACE('',#5316,0.375);
#4416=CYLINDRICAL_SURFACE('',#5328,0.225);
#4417=CYLINDRICAL_SURFACE('',#5330,0.225);
#4418=CYLINDRICAL_SURFACE('',#5332,0.225);
#4419=CYLINDRICAL_SURFACE('',#5334,1.02);
#4420=CYLINDRICAL_SURFACE('',#5336,2.1);
#4553=ADVANCED_FACE('',(#748),#4413,.F.);
#4554=ADVANCED_FACE('',(#749,#449),#553,.F.);
#4555=ADVANCED_FACE('',(#750),#4414,.F.);
#4556=ADVANCED_FACE('',(#751,#450),#554,.F.);
#4557=ADVANCED_FACE('',(#752),#4415,.F.);
#4558=ADVANCED_FACE('',(#753,#451),#555,.F.);
#4559=ADVANCED_FACE('',(#754,#452),#556,.F.);
#4560=ADVANCED_FACE('',(#755),#4416,.F.);
#4561=ADVANCED_FACE('',(#756),#4417,.F.);
#4562=ADVANCED_FACE('',(#757),#4418,.F.);
#4563=ADVANCED_FACE('',(#758),#4419,.F.);
#4564=ADVANCED_FACE('',(#759),#4420,.T.);
#4565=ADVANCED_FACE('',(#760,#453,#454,#455,#456),#557,.T.);
#4762=CLOSED_SHELL('',(#4553,#4554,#4555,#4556,#4557,#4558,#4559,#4560,
#4561,#4562,#4563,#4564,#4565));
#5303=AXIS2_PLACEMENT_3D('',#7717,#6206,#6207);
#5304=AXIS2_PLACEMENT_3D('',#7718,#6208,#6209);
#5305=AXIS2_PLACEMENT_3D('',#7723,#6211,#6212);
#5306=AXIS2_PLACEMENT_3D('',#7726,#6214,#6215);
#5307=AXIS2_PLACEMENT_3D('',#7727,#6216,#6217);
#5308=AXIS2_PLACEMENT_3D('',#7728,#6218,#6219);
#5309=AXIS2_PLACEMENT_3D('',#7730,#6220,#6221);
#5310=AXIS2_PLACEMENT_3D('',#7731,#6222,#6223);
#5311=AXIS2_PLACEMENT_3D('',#7736,#6225,#6226);
#5312=AXIS2_PLACEMENT_3D('',#7739,#6228,#6229);
#5313=AXIS2_PLACEMENT_3D('',#7740,#6230,#6231);
#5314=AXIS2_PLACEMENT_3D('',#7741,#6232,#6233);
#5315=AXIS2_PLACEMENT_3D('',#7743,#6234,#6235);
#5316=AXIS2_PLACEMENT_3D('',#7744,#6236,#6237);
#5317=AXIS2_PLACEMENT_3D('',#7749,#6239,#6240);
#5318=AXIS2_PLACEMENT_3D('',#7752,#6242,#6243);
#5319=AXIS2_PLACEMENT_3D('',#7753,#6244,#6245);
#5320=AXIS2_PLACEMENT_3D('',#7754,#6246,#6247);
#5321=AXIS2_PLACEMENT_3D('',#7756,#6248,#6249);
#5322=AXIS2_PLACEMENT_3D('',#7757,#6250,#6251);
#5323=AXIS2_PLACEMENT_3D('',#7758,#6252,#6253);
#5324=AXIS2_PLACEMENT_3D('',#7760,#6254,#6255);
#5325=AXIS2_PLACEMENT_3D('',#7761,#6256,#6257);
#5326=AXIS2_PLACEMENT_3D('',#7762,#6258,#6259);
#5327=AXIS2_PLACEMENT_3D('',#7764,#6260,#6261);
#5328=AXIS2_PLACEMENT_3D('',#7765,#6262,#6263);
#5329=AXIS2_PLACEMENT_3D('',#7768,#6265,#6266);
#5330=AXIS2_PLACEMENT_3D('',#7769,#6267,#6268);
#5331=AXIS2_PLACEMENT_3D('',#7772,#6270,#6271);
#5332=AXIS2_PLACEMENT_3D('',#7773,#6272,#6273);
#5333=AXIS2_PLACEMENT_3D('',#7776,#6275,#6276);
#5334=AXIS2_PLACEMENT_3D('',#7777,#6277,#6278);
#5335=AXIS2_PLACEMENT_3D('',#7779,#6279,#6280);
#5336=AXIS2_PLACEMENT_3D('',#7781,#6282,#6283);
#5337=AXIS2_PLACEMENT_3D('',#7783,#6284,#6285);
#5338=AXIS2_PLACEMENT_3D('',#7785,#6287,#6288);
#6206=DIRECTION('axis',(0.,0.,1.));
#6207=DIRECTION('refdir',(1.,0.,0.));
#6208=DIRECTION('center_axis',(0.,0.,1.));
#6209=DIRECTION('ref_axis',(-1.,1.22464679914735E-16,0.));
#6210=DIRECTION('',(0.,0.,-1.));
#6211=DIRECTION('center_axis',(0.,0.,1.));
#6212=DIRECTION('ref_axis',(1.,0.,0.));
#6213=DIRECTION('',(0.,0.,1.));
#6214=DIRECTION('center_axis',(0.,0.,1.));
#6215=DIRECTION('ref_axis',(1.,0.,0.));
#6216=DIRECTION('center_axis',(0.,0.,1.));
#6217=DIRECTION('ref_axis',(1.,0.,0.));
#6218=DIRECTION('center_axis',(0.,0.,1.));
#6219=DIRECTION('ref_axis',(1.,0.,0.));
#6220=DIRECTION('center_axis',(0.,0.,-1.));
#6221=DIRECTION('ref_axis',(1.,0.,0.));
#6222=DIRECTION('center_axis',(0.,0.,1.));
#6223=DIRECTION('ref_axis',(0.499999999999999,-0.866025403784439,0.));
#6224=DIRECTION('',(0.,0.,-1.));
#6225=DIRECTION('center_axis',(0.,0.,1.));
#6226=DIRECTION('ref_axis',(1.,0.,0.));
#6227=DIRECTION('',(0.,0.,1.));
#6228=DIRECTION('center_axis',(0.,0.,1.));
#6229=DIRECTION('ref_axis',(1.,0.,0.));
#6230=DIRECTION('center_axis',(0.,0.,1.));
#6231=DIRECTION('ref_axis',(1.,0.,0.));
#6232=DIRECTION('center_axis',(0.,0.,1.));
#6233=DIRECTION('ref_axis',(1.,0.,0.));
#6234=DIRECTION('center_axis',(0.,0.,-1.));
#6235=DIRECTION('ref_axis',(1.,0.,0.));
#6236=DIRECTION('center_axis',(0.,0.,1.));
#6237=DIRECTION('ref_axis',(0.500000000000001,0.866025403784438,0.));
#6238=DIRECTION('',(0.,0.,-1.));
#6239=DIRECTION('center_axis',(0.,0.,1.));
#6240=DIRECTION('ref_axis',(1.,0.,0.));
#6241=DIRECTION('',(0.,0.,1.));
#6242=DIRECTION('center_axis',(0.,0.,1.));
#6243=DIRECTION('ref_axis',(1.,0.,0.));
#6244=DIRECTION('center_axis',(0.,0.,1.));
#6245=DIRECTION('ref_axis',(1.,0.,0.));
#6246=DIRECTION('center_axis',(0.,0.,1.));
#6247=DIRECTION('ref_axis',(1.,0.,0.));
#6248=DIRECTION('center_axis',(0.,0.,-1.));
#6249=DIRECTION('ref_axis',(1.,0.,0.));
#6250=DIRECTION('center_axis',(0.,0.,1.));
#6251=DIRECTION('ref_axis',(1.,0.,0.));
#6252=DIRECTION('center_axis',(0.,0.,1.));
#6253=DIRECTION('ref_axis',(1.,0.,0.));
#6254=DIRECTION('center_axis',(0.,0.,1.));
#6255=DIRECTION('ref_axis',(1.,0.,0.));
#6256=DIRECTION('center_axis',(0.,0.,1.));
#6257=DIRECTION('ref_axis',(1.,0.,0.));
#6258=DIRECTION('center_axis',(0.,0.,1.));
#6259=DIRECTION('ref_axis',(1.,0.,0.));
#6260=DIRECTION('center_axis',(0.,0.,-1.));
#6261=DIRECTION('ref_axis',(1.,0.,0.));
#6262=DIRECTION('center_axis',(0.,0.,1.));
#6263=DIRECTION('ref_axis',(1.,0.,0.));
#6264=DIRECTION('',(0.,0.,1.));
#6265=DIRECTION('center_axis',(0.,0.,-1.));
#6266=DIRECTION('ref_axis',(1.,0.,0.));
#6267=DIRECTION('center_axis',(0.,0.,1.));
#6268=DIRECTION('ref_axis',(1.,0.,0.));
#6269=DIRECTION('',(0.,0.,1.));
#6270=DIRECTION('center_axis',(0.,0.,-1.));
#6271=DIRECTION('ref_axis',(1.,0.,0.));
#6272=DIRECTION('center_axis',(0.,0.,1.));
#6273=DIRECTION('ref_axis',(1.,0.,0.));
#6274=DIRECTION('',(0.,0.,1.));
#6275=DIRECTION('center_axis',(0.,0.,-1.));
#6276=DIRECTION('ref_axis',(1.,0.,0.));
#6277=DIRECTION('center_axis',(0.,0.,1.));
#6278=DIRECTION('ref_axis',(1.,0.,0.));
#6279=DIRECTION('center_axis',(0.,0.,-1.));
#6280=DIRECTION('ref_axis',(1.,0.,0.));
#6281=DIRECTION('',(0.,0.,-1.));
#6282=DIRECTION('center_axis',(0.,0.,1.));
#6283=DIRECTION('ref_axis',(1.,0.,0.));
#6284=DIRECTION('center_axis',(0.,0.,1.));
#6285=DIRECTION('ref_axis',(1.,0.,0.));
#6286=DIRECTION('',(0.,0.,-1.));
#6287=DIRECTION('center_axis',(0.,0.,1.));
#6288=DIRECTION('ref_axis',(1.,0.,0.));
#7717=CARTESIAN_POINT('',(0.,0.,0.));
#7718=CARTESIAN_POINT('Origin',(1.75,0.,9.9));
#7719=CARTESIAN_POINT('',(2.09482142857143,0.14738786380825,10.4));
#7720=CARTESIAN_POINT('',(2.09482142857143,0.147387863808251,10.));
#7721=CARTESIAN_POINT('',(2.09482142857143,0.14738786380825,9.9));
#7722=CARTESIAN_POINT('',(2.09482142857143,-0.14738786380825,10.4));
#7723=CARTESIAN_POINT('Origin',(1.75,0.,10.4));
#7724=CARTESIAN_POINT('',(2.09482142857143,-0.147387863808251,10.));
#7725=CARTESIAN_POINT('',(2.09482142857143,-0.14738786380825,9.9));
#7726=CARTESIAN_POINT('Origin',(1.75,0.,10.));
#7727=CARTESIAN_POINT('Origin',(1.75,0.,10.4));
#7728=CARTESIAN_POINT('Origin',(0.,0.,10.4));
#7729=CARTESIAN_POINT('',(1.525,2.75545529808155E-17,10.4));
#7730=CARTESIAN_POINT('Origin',(1.75,0.,10.4));
#7731=CARTESIAN_POINT('Origin',(-0.875,1.51554445662277,9.9));
#7732=CARTESIAN_POINT('',(-1.17505234855318,1.74047464163074,10.4));
#7733=CARTESIAN_POINT('',(-1.17505234855318,1.74047464163074,10.));
#7734=CARTESIAN_POINT('',(-1.17505234855318,1.74047464163074,9.9));
#7735=CARTESIAN_POINT('',(-0.919769080018249,1.88786250543899,10.4));
#7736=CARTESIAN_POINT('Origin',(-0.875,1.51554445662277,10.4));
#7737=CARTESIAN_POINT('',(-0.919769080018247,1.88786250543899,10.));
#7738=CARTESIAN_POINT('',(-0.919769080018249,1.88786250543899,9.9));
#7739=CARTESIAN_POINT('Origin',(-0.875,1.51554445662277,10.));
#7740=CARTESIAN_POINT('Origin',(-0.875,1.51554445662277,10.4));
#7741=CARTESIAN_POINT('Origin',(0.,0.,10.4));
#7742=CARTESIAN_POINT('',(-1.1,1.51554445662277,10.4));
#7743=CARTESIAN_POINT('Origin',(-0.875,1.51554445662277,10.4));
#7744=CARTESIAN_POINT('Origin',(-0.875000000000001,-1.51554445662277,9.9));
#7745=CARTESIAN_POINT('',(-0.91976908001825,-1.88786250543899,10.4));
#7746=CARTESIAN_POINT('',(-0.919769080018249,-1.88786250543899,10.));
#7747=CARTESIAN_POINT('',(-0.91976908001825,-1.88786250543899,9.9));
#7748=CARTESIAN_POINT('',(-1.17505234855318,-1.74047464163074,10.4));
#7749=CARTESIAN_POINT('Origin',(-0.875000000000001,-1.51554445662277,10.4));
#7750=CARTESIAN_POINT('',(-1.17505234855318,-1.74047464163074,10.));
#7751=CARTESIAN_POINT('',(-1.17505234855318,-1.74047464163074,9.9));
#7752=CARTESIAN_POINT('Origin',(-0.875000000000001,-1.51554445662277,10.));
#7753=CARTESIAN_POINT('Origin',(-0.875000000000001,-1.51554445662277,10.4));
#7754=CARTESIAN_POINT('Origin',(0.,0.,10.4));
#7755=CARTESIAN_POINT('',(-1.1,-1.51554445662277,10.4));
#7756=CARTESIAN_POINT('Origin',(-0.875000000000001,-1.51554445662277,10.4));
#7757=CARTESIAN_POINT('Origin',(0.,0.,10.));
#7758=CARTESIAN_POINT('Origin',(0.,0.,10.));
#7759=CARTESIAN_POINT('',(-2.1,-2.57175827820944E-16,10.));
#7760=CARTESIAN_POINT('Origin',(0.,0.,10.));
#7761=CARTESIAN_POINT('Origin',(0.,0.,10.));
#7762=CARTESIAN_POINT('Origin',(0.,0.,10.));
#7763=CARTESIAN_POINT('',(-1.02,-1.2491397351303E-16,10.));
#7764=CARTESIAN_POINT('Origin',(0.,0.,10.));
#7765=CARTESIAN_POINT('Origin',(1.75,0.,9.9));
#7766=CARTESIAN_POINT('',(1.525,2.75545529808155E-17,10.6));
#7767=CARTESIAN_POINT('',(1.525,-2.75545529808155E-17,9.9));
#7768=CARTESIAN_POINT('Origin',(1.75,0.,10.6));
#7769=CARTESIAN_POINT('Origin',(-0.875,1.51554445662277,9.9));
#7770=CARTESIAN_POINT('',(-1.1,1.51554445662277,10.6));
#7771=CARTESIAN_POINT('',(-1.1,1.51554445662277,9.9));
#7772=CARTESIAN_POINT('Origin',(-0.875,1.51554445662277,10.6));
#7773=CARTESIAN_POINT('Origin',(-0.875000000000001,-1.51554445662277,9.9));
#7774=CARTESIAN_POINT('',(-1.1,-1.51554445662277,10.6));
#7775=CARTESIAN_POINT('',(-1.1,-1.51554445662277,9.9));
#7776=CARTESIAN_POINT('Origin',(-0.875000000000001,-1.51554445662277,10.6));
#7777=CARTESIAN_POINT('Origin',(0.,0.,10.));
#7778=CARTESIAN_POINT('',(-1.02,-1.2491397351303E-16,10.6));
#7779=CARTESIAN_POINT('Origin',(0.,0.,10.6));
#7780=CARTESIAN_POINT('',(-1.02,-1.2491397351303E-16,10.));
#7781=CARTESIAN_POINT('Origin',(0.,0.,10.));
#7782=CARTESIAN_POINT('',(-2.1,-2.57175827820944E-16,10.6));
#7783=CARTESIAN_POINT('Origin',(0.,0.,10.6));
#7784=CARTESIAN_POINT('',(-2.1,-2.57175827820944E-16,10.));
#7785=CARTESIAN_POINT('Origin',(0.,0.,10.6));
#9752=UNCERTAINTY_MEASURE_WITH_UNIT(LENGTH_MEASURE(0.001),#9814,
'DISTANCE_ACCURACY_VALUE',
'Maximum model space distance between geometric entities at asserted c
onnectivities');
#9777=UNCERTAINTY_MEASURE_WITH_UNIT(LENGTH_MEASURE(0.001),#9814,
'DISTANCE_ACCURACY_VALUE',
'Maximum model space distance between geometric entities at asserted c
onnectivities');
#9788=(
GEOMETRIC_REPRESENTATION_CONTEXT(3)
GLOBAL_UNCERTAINTY_ASSIGNED_CONTEXT((#9752))
GLOBAL_UNIT_ASSIGNED_CONTEXT((#9814,#9816,#9817))
REPRESENTATION_CONTEXT('','3D')
);
#9813=(
GEOMETRIC_REPRESENTATION_CONTEXT(3)
GLOBAL_UNCERTAINTY_ASSIGNED_CONTEXT((#9777))
GLOBAL_UNIT_ASSIGNED_CONTEXT((#9814,#9816,#9817))
REPRESENTATION_CONTEXT('','3D')
);
#9814=(
LENGTH_UNIT()
NAMED_UNIT(*)
SI_UNIT(.CENTI.,.METRE.)
);
#9816=(
NAMED_UNIT(*)
PLANE_ANGLE_UNIT()
SI_UNIT($,.RADIAN.)
);
#9817=(
NAMED_UNIT(*)
SI_UNIT($,.STERADIAN.)
SOLID_ANGLE_UNIT()
);
#9828=SHAPE_DEFINITION_REPRESENTATION(#9863,#9945);
#9863=PRODUCT_DEFINITION_SHAPE('',$,#9981);
#9945=SHAPE_REPRESENTATION('',(#5303),#9788);
#9970=PRODUCT_DEFINITION_CONTEXT('part definition',#10077,'design');
#9981=PRODUCT_DEFINITION('Bearing retaining cap (1)',
'Bearing retaining cap (1)',#10016,#9970);
#10016=PRODUCT_DEFINITION_FORMATION('',$,#10089);
#10077=APPLICATION_CONTEXT(
'Core Data for Automotive Mechanical Design Process');
#10078=PRODUCT_CONTEXT('part definition',#10077,'mechanical');
#10089=PRODUCT('Bearing retaining cap (1)','Bearing retaining cap (1)',
'Bearing retaining cap (1)',(#10078));
#10177=COLOUR_RGB('Grey',0.48,0.52,0.57);
#10178=FILL_AREA_STYLE_COLOUR('',#10177);
#10179=FILL_AREA_STYLE('',(#10178));
#10180=SURFACE_STYLE_FILL_AREA(#10179);
#10181=SURFACE_SIDE_STYLE('',(#10180));
#10182=SURFACE_STYLE_USAGE(.BOTH.,#10181);
#10183=PRESENTATION_STYLE_ASSIGNMENT((#10182));
ENDSEC;
END-ISO-10303-21;
